ISO-10303-21;
HEADER;
/* Generated by software containing ST-Developer
 * from STEP Tools, Inc. (www.steptools.com) 
 */

FILE_DESCRIPTION(
/* description */ ('Swing-away clamp arm'),
/* implementation_level */ '2;1');

FILE_NAME(
/* name */ 'M5x14 Cap Screw.step',
/* time_stamp */ '2026-10-28T03:26:03-07:00',
/* author */ (''),
/* organization */ (''),
/* preprocessor_version */ 'ST-DEVELOPER v20.2',
/* originating_system */ 'Autodesk Translation Framework v15.17.0.0',
/* authorisation */ '');

FILE_SCHEMA (('AUTOMOTIVE_DESIGN { 1 0 10303 214 3 1 1 }'));
ENDSEC;

DATA;
#10=MECHANICAL_DESIGN_GEOMETRIC_PRESENTATION_REPRESENTATION('',(#299),#10627);
#201=CONICAL_SURFACE('',#5384,0.4,0.785398163397448);
#202=CONICAL_SURFACE('',#5388,0.41,0.785398163397448);
#203=CONICAL_SURFACE('',#5392,0.26,0.463647609000806);
#215=ORIENTED_CLOSED_SHELL('',*,#4905,.F.);
#218=BREP_WITH_VOIDS('Body1',#4906,(#215));
#247=SHAPE_REPRESENTATION_RELATIONSHIP('SRR','None',#10745,#273);
#273=ADVANCED_BREP_SHAPE_REPRESENTATION('',(#218),#10604);
#299=STYLED_ITEM('',(#10972),#218);
#384=FACE_BOUND('',#1072,.T.);
#526=PLANE('',#5372);
#527=PLANE('',#5373);
#528=PLANE('',#5374);
#529=PLANE('',#5375);
#530=PLANE('',#5376);
#531=PLANE('',#5377);
#532=PLANE('',#5378);
#533=PLANE('',#5379);
#534=PLANE('',#5380);
#535=PLANE('',#5382);
#536=PLANE('',#5390);
#725=FACE_OUTER_BOUND('',#1058,.T.);
#726=FACE_OUTER_BOUND('',#1059,.T.);
#727=FACE_OUTER_BOUND('',#1060,.T.);
#728=FACE_OUTER_BOUND('',#1061,.T.);
#729=FACE_OUTER_BOUND('',#1062,.T.);
#730=FACE_OUTER_BOUND('',#1063,.T.);
#731=FACE_OUTER_BOUND('',#1064,.T.);
#732=FACE_OUTER_BOUND('',#1065,.T.);
#733=FACE_OUTER_BOUND('',#1066,.T.);
#734=FACE_OUTER_BOUND('',#1067,.T.);
#735=FACE_OUTER_BOUND('',#1068,.T.);
#736=FACE_OUTER_BOUND('',#1069,.T.);
#737=FACE_OUTER_BOUND('',#1070,.T.);
#738=FACE_OUTER_BOUND('',#1071,.T.);
#739=FACE_OUTER_BOUND('',#1073,.T.);
#740=FACE_OUTER_BOUND('',#1074,.T.);
#1058=EDGE_LOOP('',(#3699,#3700,#3701,#3702));
#1059=EDGE_LOOP('',(#3703,#3704,#3705,#3706));
#1060=EDGE_LOOP('',(#3707,#3708,#3709,#3710));
#1061=EDGE_LOOP('',(#3711,#3712,#3713,#3714));
#1062=EDGE_LOOP('',(#3715,#3716,#3717,#3718));
#1063=EDGE_LOOP('',(#3719,#3720,#3721,#3722));
#1064=EDGE_LOOP('',(#3723,#3724,#3725,#3726,#3727,#3728));
#1065=EDGE_LOOP('',(#3729,#3730,#3731,#3732,#3733,#3734));
#1066=EDGE_LOOP('',(#3735));
#1067=EDGE_LOOP('',(#3736));
#1068=EDGE_LOOP('',(#3737,#3738,#3739,#3740));
#1069=EDGE_LOOP('',(#3741,#3742,#3743,#3744));
#1070=EDGE_LOOP('',(#3745,#3746,#3747,#3748));
#1071=EDGE_LOOP('',(#3749));
#1072=EDGE_LOOP('',(#3750));
#1073=EDGE_LOOP('',(#3751,#3752,#3753,#3754));
#1074=EDGE_LOOP('',(#3755,#3756,#3757,#3758));
#1506=LINE('',#9274,#1828);
#1507=LINE('',#9276,#1829);
#1508=LINE('',#9278,#1830);
#1509=LINE('',#9279,#1831);
#1510=LINE('',#9282,#1832);
#1511=LINE('',#9284,#1833);
#1512=LINE('',#9285,#1834);
#1513=LINE('',#9288,#1835);
#1514=LINE('',#9290,#1836);
#1515=LINE('',#9291,#1837);
#1516=LINE('',#9294,#1838);
#1517=LINE('',#9296,#1839);
#1518=LINE('',#9297,#1840);
#1519=LINE('',#9300,#1841);
#1520=LINE('',#9302,#1842);
#1521=LINE('',#9303,#1843);
#1522=LINE('',#9305,#1844);
#1523=LINE('',#9306,#1845);
#1524=LINE('',#9318,#1846);
#1525=LINE('',#9322,#1847);
#1526=LINE('',#9326,#1848);
#1527=LINE('',#9333,#1849);
#1528=LINE('',#9335,#1850);
#1828=VECTOR('',#6325,1.);
#1829=VECTOR('',#6326,1.);
#1830=VECTOR('',#6327,1.);
#1831=VECTOR('',#6328,1.);
#1832=VECTOR('',#6331,1.);
#1833=VECTOR('',#6332,1.);
#1834=VECTOR('',#6333,1.);
#1835=VECTOR('',#6336,1.);
#1836=VECTOR('',#6337,1.);
#1837=VECTOR('',#6338,1.);
#1838=VECTOR('',#6341,1.);
#1839=VECTOR('',#6342,1.);
#1840=VECTOR('',#6343,1.);
#1841=VECTOR('',#6346,1.);
#1842=VECTOR('',#6347,1.);
#1843=VECTOR('',#6348,1.);
#1844=VECTOR('',#6351,1.);
#1845=VECTOR('',#6352,1.);
#1846=VECTOR('',#6369,0.4);
#1847=VECTOR('',#6374,0.425);
#1848=VECTOR('',#6379,0.41);
#1849=VECTOR('',#6388,0.26);
#1850=VECTOR('',#6391,0.25);
#2048=CIRCLE('',#5381,0.24505);
#2049=CIRCLE('',#5383,0.375);
#2050=CIRCLE('',#5385,0.425);
#2051=CIRCLE('',#5387,0.425);
#2052=CIRCLE('',#5389,0.395);
#2053=CIRCLE('',#5391,0.27);
#2054=CIRCLE('',#5393,0.24505);
#2401=VERTEX_POINT('',#9272);
#2402=VERTEX_POINT('',#9273);
#2403=VERTEX_POINT('',#9275);
#2404=VERTEX_POINT('',#9277);
#2405=VERTEX_POINT('',#9281);
#2406=VERTEX_POINT('',#9283);
#2407=VERTEX_POINT('',#9287);
#2408=VERTEX_POINT('',#9289);
#2409=VERTEX_POINT('',#9293);
#2410=VERTEX_POINT('',#9295);
#2411=VERTEX_POINT('',#9299);
#2412=VERTEX_POINT('',#9301);
#2413=VERTEX_POINT('',#9310);
#2414=VERTEX_POINT('',#9313);
#2415=VERTEX_POINT('',#9316);
#2416=VERTEX_POINT('',#9320);
#2417=VERTEX_POINT('',#9324);
#2418=VERTEX_POINT('',#9328);
#2419=VERTEX_POINT('',#9331);
#2882=EDGE_CURVE('',#2401,#2402,#1506,.T.);
#2883=EDGE_CURVE('',#2402,#2403,#1507,.T.);
#2884=EDGE_CURVE('',#2403,#2404,#1508,.T.);
#2885=EDGE_CURVE('',#2401,#2404,#1509,.T.);
#2886=EDGE_CURVE('',#2402,#2405,#1510,.T.);
#2887=EDGE_CURVE('',#2405,#2406,#1511,.T.);
#2888=EDGE_CURVE('',#2406,#2403,#1512,.T.);
#2889=EDGE_CURVE('',#2405,#2407,#1513,.T.);
#2890=EDGE_CURVE('',#2407,#2408,#1514,.T.);
#2891=EDGE_CURVE('',#2408,#2406,#1515,.T.);
#2892=EDGE_CURVE('',#2407,#2409,#1516,.T.);
#2893=EDGE_CURVE('',#2409,#2410,#1517,.T.);
#2894=EDGE_CURVE('',#2410,#2408,#1518,.T.);
#2895=EDGE_CURVE('',#2409,#2411,#1519,.T.);
#2896=EDGE_CURVE('',#2411,#2412,#1520,.T.);
#2897=EDGE_CURVE('',#2412,#2410,#1521,.T.);
#2898=EDGE_CURVE('',#2411,#2401,#1522,.T.);
#2899=EDGE_CURVE('',#2404,#2412,#1523,.T.);
#2900=EDGE_CURVE('',#2413,#2413,#2048,.T.);
#2901=EDGE_CURVE('',#2414,#2414,#2049,.T.);
#2902=EDGE_CURVE('',#2415,#2415,#2050,.T.);
#2903=EDGE_CURVE('',#2415,#2414,#1524,.T.);
#2904=EDGE_CURVE('',#2416,#2416,#2051,.T.);
#2905=EDGE_CURVE('',#2416,#2415,#1525,.T.);
#2906=EDGE_CURVE('',#2417,#2417,#2052,.T.);
#2907=EDGE_CURVE('',#2417,#2416,#1526,.T.);
#2908=EDGE_CURVE('',#2418,#2418,#2053,.T.);
#2909=EDGE_CURVE('',#2419,#2419,#2054,.F.);
#2910=EDGE_CURVE('',#2419,#2418,#1527,.T.);
#2911=EDGE_CURVE('',#2413,#2419,#1528,.T.);
#3699=ORIENTED_EDGE('',*,*,#2882,.T.);
#3700=ORIENTED_EDGE('',*,*,#2883,.T.);
#3701=ORIENTED_EDGE('',*,*,#2884,.T.);
#3702=ORIENTED_EDGE('',*,*,#2885,.F.);
#3703=ORIENTED_EDGE('',*,*,#2886,.T.);
#3704=ORIENTED_EDGE('',*,*,#2887,.T.);
#3705=ORIENTED_EDGE('',*,*,#2888,.T.);
#3706=ORIENTED_EDGE('',*,*,#2883,.F.);
#3707=ORIENTED_EDGE('',*,*,#2889,.T.);
#3708=ORIENTED_EDGE('',*,*,#2890,.T.);
#3709=ORIENTED_EDGE('',*,*,#2891,.T.);
#3710=ORIENTED_EDGE('',*,*,#2887,.F.);
#3711=ORIENTED_EDGE('',*,*,#2892,.T.);
#3712=ORIENTED_EDGE('',*,*,#2893,.T.);
#3713=ORIENTED_EDGE('',*,*,#2894,.T.);
#3714=ORIENTED_EDGE('',*,*,#2890,.F.);
#3715=ORIENTED_EDGE('',*,*,#2895,.T.);
#3716=ORIENTED_EDGE('',*,*,#2896,.T.);
#3717=ORIENTED_EDGE('',*,*,#2897,.T.);
#3718=ORIENTED_EDGE('',*,*,#2893,.F.);
#3719=ORIENTED_EDGE('',*,*,#2898,.T.);
#3720=ORIENTED_EDGE('',*,*,#2885,.T.);
#3721=ORIENTED_EDGE('',*,*,#2899,.T.);
#3722=ORIENTED_EDGE('',*,*,#2896,.F.);
#3723=ORIENTED_EDGE('',*,*,#2898,.F.);
#3724=ORIENTED_EDGE('',*,*,#2895,.F.);
#3725=ORIENTED_EDGE('',*,*,#2892,.F.);
#3726=ORIENTED_EDGE('',*,*,#2889,.F.);
#3727=ORIENTED_EDGE('',*,*,#2886,.F.);
#3728=ORIENTED_EDGE('',*,*,#2882,.F.);
#3729=ORIENTED_EDGE('',*,*,#2899,.F.);
#3730=ORIENTED_EDGE('',*,*,#2884,.F.);
#3731=ORIENTED_EDGE('',*,*,#2888,.F.);
#3732=ORIENTED_EDGE('',*,*,#2891,.F.);
#3733=ORIENTED_EDGE('',*,*,#2894,.F.);
#3734=ORIENTED_EDGE('',*,*,#2897,.F.);
#3735=ORIENTED_EDGE('',*,*,#2900,.F.);
#3736=ORIENTED_EDGE('',*,*,#2901,.F.);
#3737=ORIENTED_EDGE('',*,*,#2902,.F.);
#3738=ORIENTED_EDGE('',*,*,#2903,.T.);
#3739=ORIENTED_EDGE('',*,*,#2901,.T.);
#3740=ORIENTED_EDGE('',*,*,#2903,.F.);
#3741=ORIENTED_EDGE('',*,*,#2904,.F.);
#3742=ORIENTED_EDGE('',*,*,#2905,.T.);
#3743=ORIENTED_EDGE('',*,*,#2902,.T.);
#3744=ORIENTED_EDGE('',*,*,#2905,.F.);
#3745=ORIENTED_EDGE('',*,*,#2906,.F.);
#3746=ORIENTED_EDGE('',*,*,#2907,.T.);
#3747=ORIENTED_EDGE('',*,*,#2904,.T.);
#3748=ORIENTED_EDGE('',*,*,#2907,.F.);
#3749=ORIENTED_EDGE('',*,*,#2906,.T.);
#3750=ORIENTED_EDGE('',*,*,#2908,.F.);
#3751=ORIENTED_EDGE('',*,*,#2909,.F.);
#3752=ORIENTED_EDGE('',*,*,#2910,.T.);
#3753=ORIENTED_EDGE('',*,*,#2908,.T.);
#3754=ORIENTED_EDGE('',*,*,#2910,.F.);
#3755=ORIENTED_EDGE('',*,*,#2900,.T.);
#3756=ORIENTED_EDGE('',*,*,#2911,.T.);
#3757=ORIENTED_EDGE('',*,*,#2909,.T.);
#3758=ORIENTED_EDGE('',*,*,#2911,.F.);
#4516=CYLINDRICAL_SURFACE('',#5386,0.425);
#4517=CYLINDRICAL_SURFACE('',#5394,0.24505);
#4680=ADVANCED_FACE('',(#725),#526,.F.);
#4681=ADVANCED_FACE('',(#726),#527,.F.);
#4682=ADVANCED_FACE('',(#727),#528,.F.);
#4683=ADVANCED_FACE('',(#728),#529,.F.);
#4684=ADVANCED_FACE('',(#729),#530,.F.);
#4685=ADVANCED_FACE('',(#730),#531,.F.);
#4686=ADVANCED_FACE('',(#731),#532,.F.);
#4687=ADVANCED_FACE('',(#732),#533,.F.);
#4688=ADVANCED_FACE('',(#733),#534,.F.);
#4689=ADVANCED_FACE('',(#734),#535,.T.);
#4690=ADVANCED_FACE('',(#735),#201,.T.);
#4691=ADVANCED_FACE('',(#736),#4516,.T.);
#4692=ADVANCED_FACE('',(#737),#202,.T.);
#4693=ADVANCED_FACE('',(#738,#384),#536,.T.);
#4694=ADVANCED_FACE('',(#739),#203,.T.);
#4695=ADVANCED_FACE('',(#740),#4517,.T.);
#4905=CLOSED_SHELL('',(#4680,#4681,#4682,#4683,#4684,#4685,#4686,#4687));
#4906=CLOSED_SHELL('',(#4688,#4689,#4690,#4691,#4692,#4693,#4694,#4695));
#5371=AXIS2_PLACEMENT_3D('',#9270,#6321,#6322);
#5372=AXIS2_PLACEMENT_3D('',#9271,#6323,#6324);
#5373=AXIS2_PLACEMENT_3D('',#9280,#6329,#6330);
#5374=AXIS2_PLACEMENT_3D('',#9286,#6334,#6335);
#5375=AXIS2_PLACEMENT_3D('',#9292,#6339,#6340);
#5376=AXIS2_PLACEMENT_3D('',#9298,#6344,#6345);
#5377=AXIS2_PLACEMENT_3D('',#9304,#6349,#6350);
#5378=AXIS2_PLACEMENT_3D('',#9307,#6353,#6354);
#5379=AXIS2_PLACEMENT_3D('',#9308,#6355,#6356);
#5380=AXIS2_PLACEMENT_3D('',#9309,#6357,#6358);
#5381=AXIS2_PLACEMENT_3D('',#9311,#6359,#6360);
#5382=AXIS2_PLACEMENT_3D('',#9312,#6361,#6362);
#5383=AXIS2_PLACEMENT_3D('',#9314,#6363,#6364);
#5384=AXIS2_PLACEMENT_3D('',#9315,#6365,#6366);
#5385=AXIS2_PLACEMENT_3D('',#9317,#6367,#6368);
#5386=AXIS2_PLACEMENT_3D('',#9319,#6370,#6371);
#5387=AXIS2_PLACEMENT_3D('',#9321,#6372,#6373);
#5388=AXIS2_PLACEMENT_3D('',#9323,#6375,#6376);
#5389=AXIS2_PLACEMENT_3D('',#9325,#6377,#6378);
#5390=AXIS2_PLACEMENT_3D('',#9327,#6380,#6381);
#5391=AXIS2_PLACEMENT_3D('',#9329,#6382,#6383);
#5392=AXIS2_PLACEMENT_3D('',#9330,#6384,#6385);
#5393=AXIS2_PLACEMENT_3D('',#9332,#6386,#6387);
#5394=AXIS2_PLACEMENT_3D('',#9334,#6389,#6390);
#6321=DIRECTION('axis',(0.,0.,1.));
#6322=DIRECTION('refdir',(1.,0.,0.));
#6323=DIRECTION('center_axis',(0.866025403784439,0.,-0.5));
#6324=DIRECTION('ref_axis',(0.5,0.,0.866025403784439));
#6325=DIRECTION('',(-0.5,0.,-0.866025403784439));
#6326=DIRECTION('',(0.,-1.,0.));
#6327=DIRECTION('',(0.5,0.,0.866025403784439));
#6328=DIRECTION('',(0.,-1.,0.));
#6329=DIRECTION('center_axis',(1.20185167898973E-16,0.,-1.));
#6330=DIRECTION('ref_axis',(1.,0.,1.20185167898973E-16));
#6331=DIRECTION('',(-1.,0.,-1.20185167898973E-16));
#6332=DIRECTION('',(0.,-1.,0.));
#6333=DIRECTION('',(1.,0.,1.20185167898973E-16));
#6334=DIRECTION('center_axis',(-0.866025403784439,0.,-0.5));
#6335=DIRECTION('ref_axis',(0.5,0.,-0.866025403784439));
#6336=DIRECTION('',(-0.5,0.,0.866025403784439));
#6337=DIRECTION('',(0.,-1.,0.));
#6338=DIRECTION('',(0.5,0.,-0.866025403784439));
#6339=DIRECTION('center_axis',(-0.866025403784439,0.,0.5));
#6340=DIRECTION('ref_axis',(-0.5,0.,-0.866025403784439));
#6341=DIRECTION('',(0.5,0.,0.866025403784439));
#6342=DIRECTION('',(0.,-1.,0.));
#6343=DIRECTION('',(-0.5,0.,-0.866025403784439));
#6344=DIRECTION('center_axis',(-2.40370335797945E-16,0.,1.));
#6345=DIRECTION('ref_axis',(-1.,0.,-2.40370335797945E-16));
#6346=DIRECTION('',(1.,0.,2.40370335797945E-16));
#6347=DIRECTION('',(0.,-1.,0.));
#6348=DIRECTION('',(-1.,0.,-2.40370335797945E-16));
#6349=DIRECTION('center_axis',(0.866025403784439,0.,0.5));
#6350=DIRECTION('ref_axis',(-0.5,0.,0.866025403784439));
#6351=DIRECTION('',(0.5,0.,-0.866025403784439));
#6352=DIRECTION('',(-0.5,0.,0.866025403784439));
#6353=DIRECTION('center_axis',(0.,1.,0.));
#6354=DIRECTION('ref_axis',(1.,0.,0.));
#6355=DIRECTION('center_axis',(0.,-1.,0.));
#6356=DIRECTION('ref_axis',(0.,0.,-1.));
#6357=DIRECTION('center_axis',(0.,1.,0.));
#6358=DIRECTION('ref_axis',(1.,0.,0.));
#6359=DIRECTION('center_axis',(0.,1.,0.));
#6360=DIRECTION('ref_axis',(1.,0.,0.));
#6361=DIRECTION('center_axis',(0.,1.,0.));
#6362=DIRECTION('ref_axis',(0.,0.,1.));
#6363=DIRECTION('center_axis',(0.,-1.,0.));
#6364=DIRECTION('ref_axis',(1.,0.,0.));
#6365=DIRECTION('center_axis',(0.,-1.,0.));
#6366=DIRECTION('ref_axis',(1.,0.,0.));
#6367=DIRECTION('center_axis',(0.,-1.,0.));
#6368=DIRECTION('ref_axis',(1.,0.,0.));
#6369=DIRECTION('',(0.707106781186548,0.707106781186547,8.65956056235493E-17));
#6370=DIRECTION('center_axis',(0.,-1.,0.));
#6371=DIRECTION('ref_axis',(1.,0.,0.));
#6372=DIRECTION('center_axis',(0.,-1.,0.));
#6373=DIRECTION('ref_axis',(1.,0.,0.));
#6374=DIRECTION('',(0.,1.,0.));
#6375=DIRECTION('center_axis',(0.,1.,0.));
#6376=DIRECTION('ref_axis',(1.,0.,0.));
#6377=DIRECTION('center_axis',(0.,-1.,0.));
#6378=DIRECTION('ref_axis',(1.,0.,0.));
#6379=DIRECTION('',(-0.707106781186547,0.707106781186548,-8.65956056235493E-17));
#6380=DIRECTION('center_axis',(0.,-1.,0.));
#6381=DIRECTION('ref_axis',(0.,0.,-1.));
#6382=DIRECTION('center_axis',(0.,-1.,0.));
#6383=DIRECTION('ref_axis',(1.,0.,0.));
#6384=DIRECTION('center_axis',(0.,1.,0.));
#6385=DIRECTION('ref_axis',(1.,0.,0.));
#6386=DIRECTION('center_axis',(0.,1.,0.));
#6387=DIRECTION('ref_axis',(1.,0.,0.));
#6388=DIRECTION('',(-0.447213595499958,0.894427190999916,-5.47678698264203E-17));
#6389=DIRECTION('center_axis',(0.,-1.,0.));
#6390=DIRECTION('ref_axis',(1.,0.,0.));
#6391=DIRECTION('',(0.,1.,0.));
#9270=CARTESIAN_POINT('',(0.,0.,0.));
#9271=CARTESIAN_POINT('Origin',(0.115470053837925,-1.,-0.2));
#9272=CARTESIAN_POINT('',(0.23094010767585,-1.,-1.11022302462516E-16));
#9273=CARTESIAN_POINT('',(0.115470053837925,-1.,-0.2));
#9274=CARTESIAN_POINT('',(0.23094010767585,-1.,-1.11022302462516E-16));
#9275=CARTESIAN_POINT('',(0.115470053837925,-1.3,-0.2));
#9276=CARTESIAN_POINT('',(0.115470053837925,-1.,-0.2));
#9277=CARTESIAN_POINT('',(0.23094010767585,-1.3,-1.11022302462516E-16));
#9278=CARTESIAN_POINT('',(0.23094010767585,-1.3,-1.11022302462516E-16));
#9279=CARTESIAN_POINT('',(0.23094010767585,-1.,-1.11022302462516E-16));
#9280=CARTESIAN_POINT('Origin',(-0.115470053837925,-1.,-0.2));
#9281=CARTESIAN_POINT('',(-0.115470053837925,-1.,-0.2));
#9282=CARTESIAN_POINT('',(0.115470053837925,-1.,-0.2));
#9283=CARTESIAN_POINT('',(-0.115470053837925,-1.3,-0.2));
#9284=CARTESIAN_POINT('',(-0.115470053837925,-1.,-0.2));
#9285=CARTESIAN_POINT('',(0.115470053837925,-1.3,-0.2));
#9286=CARTESIAN_POINT('Origin',(-0.23094010767585,-1.,-1.38777878078145E-16));
#9287=CARTESIAN_POINT('',(-0.23094010767585,-1.,-1.39304308828513E-16));
#9288=CARTESIAN_POINT('',(-0.115470053837925,-1.,-0.2));
#9289=CARTESIAN_POINT('',(-0.23094010767585,-1.3,-1.38777878078145E-16));
#9290=CARTESIAN_POINT('',(-0.23094010767585,-1.,-1.39304308828513E-16));
#9291=CARTESIAN_POINT('',(-0.115470053837925,-1.3,-0.2));
#9292=CARTESIAN_POINT('Origin',(-0.115470053837925,-1.,0.2));
#9293=CARTESIAN_POINT('',(-0.115470053837925,-1.,0.2));
#9294=CARTESIAN_POINT('',(-0.23094010767585,-1.,-1.39304308828513E-16));
#9295=CARTESIAN_POINT('',(-0.115470053837925,-1.3,0.2));
#9296=CARTESIAN_POINT('',(-0.115470053837925,-1.,0.2));
#9297=CARTESIAN_POINT('',(-0.23094010767585,-1.3,-1.39304308828513E-16));
#9298=CARTESIAN_POINT('Origin',(0.115470053837925,-1.,0.2));
#9299=CARTESIAN_POINT('',(0.115470053837925,-1.,0.2));
#9300=CARTESIAN_POINT('',(-0.115470053837925,-1.,0.2));
#9301=CARTESIAN_POINT('',(0.115470053837925,-1.3,0.2));
#9302=CARTESIAN_POINT('',(0.115470053837925,-1.,0.2));
#9303=CARTESIAN_POINT('',(-0.115470053837925,-1.3,0.2));
#9304=CARTESIAN_POINT('Origin',(0.23094010767585,-1.,-1.11022302462516E-16));
#9305=CARTESIAN_POINT('',(0.115470053837925,-1.,0.2));
#9306=CARTESIAN_POINT('',(0.115470053837925,-1.3,0.2));
#9307=CARTESIAN_POINT('Origin',(0.,-1.,-1.11022302462516E-16));
#9308=CARTESIAN_POINT('Origin',(0.,-1.3,-1.11022302462516E-16));
#9309=CARTESIAN_POINT('Origin',(0.,-1.9,-1.11022302462516E-16));
#9310=CARTESIAN_POINT('',(-0.24505,-1.9,-8.10123326494098E-17));
#9311=CARTESIAN_POINT('Origin',(0.,-1.9,-1.11022302462516E-16));
#9312=CARTESIAN_POINT('Origin',(0.375,0.,-1.11022302462516E-16));
#9313=CARTESIAN_POINT('',(-0.375,5.20417042793042E-17,-1.56946557430541E-16));
#9314=CARTESIAN_POINT('Origin',(0.,0.,-1.11022302462516E-16));
#9315=CARTESIAN_POINT('Origin',(0.,-0.0249999999999999,-1.11022302462516E-16));
#9316=CARTESIAN_POINT('',(-0.425,-0.0499999999999999,-1.63069791426278E-16));
#9317=CARTESIAN_POINT('Origin',(0.,-0.0499999999999998,-1.11022302462516E-16));
#9318=CARTESIAN_POINT('',(-0.4,-0.0249999999999999,-1.6000817442841E-16));
#9319=CARTESIAN_POINT('Origin',(0.,-0.26,-1.11022302462516E-16));
#9320=CARTESIAN_POINT('',(-0.425,-0.47,-1.63069791426278E-16));
#9321=CARTESIAN_POINT('Origin',(0.,-0.47,-1.11022302462516E-16));
#9322=CARTESIAN_POINT('',(-0.425,-0.26,-1.63069791426278E-16));
#9323=CARTESIAN_POINT('Origin',(0.,-0.485,-1.11022302462516E-16));
#9324=CARTESIAN_POINT('',(-0.395,-0.5,-1.59395851028836E-16));
#9325=CARTESIAN_POINT('Origin',(0.,-0.5,-1.11022302462516E-16));
#9326=CARTESIAN_POINT('',(-0.41,-0.485,-1.61232821227557E-16));
#9327=CARTESIAN_POINT('Origin',(0.27,-0.5,-1.11022302462516E-16));
#9328=CARTESIAN_POINT('',(-0.27,-0.5,-1.44087766039494E-16));
#9329=CARTESIAN_POINT('Origin',(0.,-0.5,-1.11022302462516E-16));
#9330=CARTESIAN_POINT('Origin',(0.,-0.52,-1.11022302462516E-16));
#9331=CARTESIAN_POINT('',(-0.24505,-0.5499,-8.10123326494098E-17));
#9332=CARTESIAN_POINT('Origin',(0.,-0.5499,-1.11022302462516E-16));
#9333=CARTESIAN_POINT('',(-0.26,-0.52,-1.42863119240347E-16));
#9334=CARTESIAN_POINT('Origin',(0.,-1.495,-1.11022302462516E-16));
#9335=CARTESIAN_POINT('',(-0.24505,-1.495,-1.41032272275622E-16));
#10572=UNCERTAINTY_MEASURE_WITH_UNIT(LENGTH_MEASURE(0.001),#10628,
'DISTANCE_ACCURACY_VALUE',
'Maximum model space distance between geometric entities at asserted c
onnectivities');
#10595=UNCERTAINTY_MEASURE_WITH_UNIT(LENGTH_MEASURE(0.001),#10628,
'DISTANCE_ACCURACY_VALUE',
'Maximum model space distance between geometric entities at asserted c
onnectivities');
#10604=(
GEOMETRIC_REPRESENTATION_CONTEXT(3)
GLOBAL_UNCERTAINTY_ASSIGNED_CONTEXT((#10572))
GLOBAL_UNIT_ASSIGNED_CONTEXT((#10628,#10630,#10631))
REPRESENTATION_CONTEXT('','3D')
);
#10627=(
GEOMETRIC_REPRESENTATION_CONTEXT(3)
GLOBAL_UNCERTAINTY_ASSIGNED_CONTEXT((#10595))
GLOBAL_UNIT_ASSIGNED_CONTEXT((#10628,#10630,#10631))
REPRESENTATION_CONTEXT('','3D')
);
#10628=(
LENGTH_UNIT()
NAMED_UNIT(*)
SI_UNIT(.CENTI.,.METRE.)
);
#10630=(
NAMED_UNIT(*)
PLANE_ANGLE_UNIT()
SI_UNIT($,.RADIAN.)
);
#10631=(
NAMED_UNIT(*)
SI_UNIT($,.STERADIAN.)
SOLID_ANGLE_UNIT()
);
#10640=SHAPE_DEFINITION_REPRESENTATION(#10671,#10745);
#10671=PRODUCT_DEFINITION_SHAPE('',$,#10777);
#10745=SHAPE_REPRESENTATION('',(#5371),#10604);
#10768=PRODUCT_DEFINITION_CONTEXT('part definition',#10863,'design');
#10777=PRODUCT_DEFINITION('M5x14 Cap Screw','M5x14 Cap Screw',#10808,#10768);
#10808=PRODUCT_DEFINITION_FORMATION('',$,#10873);
#10863=APPLICATION_CONTEXT(
'Core Data for Automotive Mechanical Design Process');
#10864=PRODUCT_CONTEXT('part definition',#10863,'mechanical');
#10873=PRODUCT('M5x14 Cap Screw','M5x14 Cap Screw','M5x14 Cap Screw',(#10864));
#10966=COLOUR_RGB('Black',0.12,0.14,0.17);
#10967=FILL_AREA_STYLE_COLOUR('',#10966);
#10968=FILL_AREA_STYLE('',(#10967));
#10969=SURFACE_STYLE_FILL_AREA(#10968);
#10970=SURFACE_SIDE_STYLE('',(#10969));
#10971=SURFACE_STYLE_USAGE(.BOTH.,#10970);
#10972=PRESENTATION_STYLE_ASSIGNMENT((#10971));
ENDSEC;
END-ISO-10303-21;
